ISO-10303-21;
HEADER;
/* Generated by software containing ST-Developer
 * from STEP Tools, Inc. (www.steptools.com) 
 */

FILE_DESCRIPTION(
/* description */ ('Hand-crank flanged shaft unit'),
/* implementation_level */ '2;1');

FILE_NAME(
/* name */ 'Cap Screw - M8x30.step',
/* time_stamp */ '2026-10-27T18:35:45-07:00',
/* author */ (''),
/* organization */ (''),
/* preprocessor_version */ 'ST-DEVELOPER v20.2',
/* originating_system */ 'Autodesk Translation Framework v15.17.0.0',
/* authorisation */ '');

FILE_SCHEMA (('AUTOMOTIVE_DESIGN { 1 0 10303 214 3 1 1 }'));
ENDSEC;

DATA;
#10=MECHANICAL_DESIGN_GEOMETRIC_PRESENTATION_REPRESENTATION('',(#292),#6805);
#12=ORIENTED_CLOSED_SHELL('',*,#3334,.F.);
#13=CONICAL_SURFACE('',#3755,0.625,0.785398163397448);
#14=CONICAL_SURFACE('',#3759,0.635,0.785398163397449);
#15=CONICAL_SURFACE('',#3763,0.41,0.463647609000806);
#16=CONICAL_SURFACE('',#3767,0.36,0.785398163397448);
#28=BREP_WITH_VOIDS('Body1',#3333,(#12));
#251=SHAPE_REPRESENTATION_RELATIONSHIP('SRR','None',#6913,#271);
#271=ADVANCED_BREP_SHAPE_REPRESENTATION('',(#28),#6796);
#292=STYLED_ITEM('',(#7098),#28);
#393=FACE_BOUND('',#880,.T.);
#461=PLANE('',#3753);
#462=PLANE('',#3761);
#463=PLANE('',#3769);
#464=PLANE('',#3770);
#465=PLANE('',#3771);
#466=PLANE('',#3772);
#467=PLANE('',#3773);
#468=PLANE('',#3774);
#469=PLANE('',#3775);
#470=PLANE('',#3776);
#471=PLANE('',#3777);
#614=FACE_OUTER_BOUND('',#875,.T.);
#615=FACE_OUTER_BOUND('',#876,.T.);
#616=FACE_OUTER_BOUND('',#877,.T.);
#617=FACE_OUTER_BOUND('',#878,.T.);
#618=FACE_OUTER_BOUND('',#879,.T.);
#619=FACE_OUTER_BOUND('',#881,.T.);
#620=FACE_OUTER_BOUND('',#882,.T.);
#621=FACE_OUTER_BOUND('',#883,.T.);
#622=FACE_OUTER_BOUND('',#884,.T.);
#623=FACE_OUTER_BOUND('',#885,.T.);
#624=FACE_OUTER_BOUND('',#886,.T.);
#625=FACE_OUTER_BOUND('',#887,.T.);
#626=FACE_OUTER_BOUND('',#888,.T.);
#627=FACE_OUTER_BOUND('',#889,.T.);
#628=FACE_OUTER_BOUND('',#890,.T.);
#629=FACE_OUTER_BOUND('',#891,.T.);
#630=FACE_OUTER_BOUND('',#892,.T.);
#875=EDGE_LOOP('',(#2679));
#876=EDGE_LOOP('',(#2680,#2681,#2682,#2683));
#877=EDGE_LOOP('',(#2684,#2685,#2686,#2687));
#878=EDGE_LOOP('',(#2688,#2689,#2690,#2691));
#879=EDGE_LOOP('',(#2692));
#880=EDGE_LOOP('',(#2693));
#881=EDGE_LOOP('',(#2694,#2695,#2696,#2697));
#882=EDGE_LOOP('',(#2698,#2699,#2700,#2701));
#883=EDGE_LOOP('',(#2702,#2703,#2704,#2705));
#884=EDGE_LOOP('',(#2706));
#885=EDGE_LOOP('',(#2707,#2708,#2709,#2710));
#886=EDGE_LOOP('',(#2711,#2712,#2713,#2714));
#887=EDGE_LOOP('',(#2715,#2716,#2717,#2718));
#888=EDGE_LOOP('',(#2719,#2720,#2721,#2722));
#889=EDGE_LOOP('',(#2723,#2724,#2725,#2726));
#890=EDGE_LOOP('',(#2727,#2728,#2729,#2730));
#891=EDGE_LOOP('',(#2731,#2732,#2733,#2734,#2735,#2736));
#892=EDGE_LOOP('',(#2737,#2738,#2739,#2740,#2741,#2742));
#1087=LINE('',#5827,#1315);
#1088=LINE('',#5831,#1316);
#1089=LINE('',#5835,#1317);
#1090=LINE('',#5842,#1318);
#1091=LINE('',#5846,#1319);
#1092=LINE('',#5850,#1320);
#1093=LINE('',#5855,#1321);
#1094=LINE('',#5857,#1322);
#1095=LINE('',#5859,#1323);
#1096=LINE('',#5860,#1324);
#1097=LINE('',#5863,#1325);
#1098=LINE('',#5865,#1326);
#1099=LINE('',#5866,#1327);
#1100=LINE('',#5869,#1328);
#1101=LINE('',#5871,#1329);
#1102=LINE('',#5872,#1330);
#1103=LINE('',#5875,#1331);
#1104=LINE('',#5877,#1332);
#1105=LINE('',#5878,#1333);
#1106=LINE('',#5881,#1334);
#1107=LINE('',#5883,#1335);
#1108=LINE('',#5884,#1336);
#1109=LINE('',#5886,#1337);
#1110=LINE('',#5887,#1338);
#1315=VECTOR('',#4452,0.625);
#1316=VECTOR('',#4457,0.65);
#1317=VECTOR('',#4462,0.635);
#1318=VECTOR('',#4471,0.41);
#1319=VECTOR('',#4476,0.4);
#1320=VECTOR('',#4481,0.36);
#1321=VECTOR('',#4486,1.);
#1322=VECTOR('',#4487,1.);
#1323=VECTOR('',#4488,1.);
#1324=VECTOR('',#4489,1.);
#1325=VECTOR('',#4492,1.);
#1326=VECTOR('',#4493,1.);
#1327=VECTOR('',#4494,1.);
#1328=VECTOR('',#4497,1.);
#1329=VECTOR('',#4498,1.);
#1330=VECTOR('',#4499,1.);
#1331=VECTOR('',#4502,1.);
#1332=VECTOR('',#4503,1.);
#1333=VECTOR('',#4504,1.);
#1334=VECTOR('',#4507,1.);
#1335=VECTOR('',#4508,1.);
#1336=VECTOR('',#4509,1.);
#1337=VECTOR('',#4512,1.);
#1338=VECTOR('',#4513,1.);
#1521=CIRCLE('',#3754,0.6);
#1522=CIRCLE('',#3756,0.65);
#1523=CIRCLE('',#3758,0.65);
#1524=CIRCLE('',#3760,0.62);
#1525=CIRCLE('',#3762,0.42);
#1526=CIRCLE('',#3764,0.3933);
#1527=CIRCLE('',#3766,0.3933);
#1528=CIRCLE('',#3768,0.32);
#1719=VERTEX_POINT('',#5822);
#1720=VERTEX_POINT('',#5825);
#1721=VERTEX_POINT('',#5829);
#1722=VERTEX_POINT('',#5833);
#1723=VERTEX_POINT('',#5837);
#1724=VERTEX_POINT('',#5840);
#1725=VERTEX_POINT('',#5844);
#1726=VERTEX_POINT('',#5848);
#1727=VERTEX_POINT('',#5853);
#1728=VERTEX_POINT('',#5854);
#1729=VERTEX_POINT('',#5856);
#1730=VERTEX_POINT('',#5858);
#1731=VERTEX_POINT('',#5862);
#1732=VERTEX_POINT('',#5864);
#1733=VERTEX_POINT('',#5868);
#1734=VERTEX_POINT('',#5870);
#1735=VERTEX_POINT('',#5874);
#1736=VERTEX_POINT('',#5876);
#1737=VERTEX_POINT('',#5880);
#1738=VERTEX_POINT('',#5882);
#2057=EDGE_CURVE('',#1719,#1719,#1521,.T.);
#2058=EDGE_CURVE('',#1720,#1720,#1522,.T.);
#2059=EDGE_CURVE('',#1720,#1719,#1087,.T.);
#2060=EDGE_CURVE('',#1721,#1721,#1523,.T.);
#2061=EDGE_CURVE('',#1721,#1720,#1088,.T.);
#2062=EDGE_CURVE('',#1722,#1722,#1524,.T.);
#2063=EDGE_CURVE('',#1722,#1721,#1089,.T.);
#2064=EDGE_CURVE('',#1723,#1723,#1525,.T.);
#2065=EDGE_CURVE('',#1724,#1724,#1526,.F.);
#2066=EDGE_CURVE('',#1724,#1723,#1090,.T.);
#2067=EDGE_CURVE('',#1725,#1725,#1527,.F.);
#2068=EDGE_CURVE('',#1725,#1724,#1091,.T.);
#2069=EDGE_CURVE('',#1726,#1726,#1528,.T.);
#2070=EDGE_CURVE('',#1726,#1725,#1092,.T.);
#2071=EDGE_CURVE('',#1727,#1728,#1093,.T.);
#2072=EDGE_CURVE('',#1728,#1729,#1094,.T.);
#2073=EDGE_CURVE('',#1729,#1730,#1095,.T.);
#2074=EDGE_CURVE('',#1727,#1730,#1096,.T.);
#2075=EDGE_CURVE('',#1728,#1731,#1097,.T.);
#2076=EDGE_CURVE('',#1731,#1732,#1098,.T.);
#2077=EDGE_CURVE('',#1732,#1729,#1099,.T.);
#2078=EDGE_CURVE('',#1731,#1733,#1100,.T.);
#2079=EDGE_CURVE('',#1733,#1734,#1101,.T.);
#2080=EDGE_CURVE('',#1734,#1732,#1102,.T.);
#2081=EDGE_CURVE('',#1733,#1735,#1103,.T.);
#2082=EDGE_CURVE('',#1735,#1736,#1104,.T.);
#2083=EDGE_CURVE('',#1736,#1734,#1105,.T.);
#2084=EDGE_CURVE('',#1735,#1737,#1106,.T.);
#2085=EDGE_CURVE('',#1737,#1738,#1107,.T.);
#2086=EDGE_CURVE('',#1738,#1736,#1108,.T.);
#2087=EDGE_CURVE('',#1737,#1727,#1109,.T.);
#2088=EDGE_CURVE('',#1730,#1738,#1110,.T.);
#2679=ORIENTED_EDGE('',*,*,#2057,.F.);
#2680=ORIENTED_EDGE('',*,*,#2058,.F.);
#2681=ORIENTED_EDGE('',*,*,#2059,.T.);
#2682=ORIENTED_EDGE('',*,*,#2057,.T.);
#2683=ORIENTED_EDGE('',*,*,#2059,.F.);
#2684=ORIENTED_EDGE('',*,*,#2060,.F.);
#2685=ORIENTED_EDGE('',*,*,#2061,.T.);
#2686=ORIENTED_EDGE('',*,*,#2058,.T.);
#2687=ORIENTED_EDGE('',*,*,#2061,.F.);
#2688=ORIENTED_EDGE('',*,*,#2062,.F.);
#2689=ORIENTED_EDGE('',*,*,#2063,.T.);
#2690=ORIENTED_EDGE('',*,*,#2060,.T.);
#2691=ORIENTED_EDGE('',*,*,#2063,.F.);
#2692=ORIENTED_EDGE('',*,*,#2062,.T.);
#2693=ORIENTED_EDGE('',*,*,#2064,.F.);
#2694=ORIENTED_EDGE('',*,*,#2065,.F.);
#2695=ORIENTED_EDGE('',*,*,#2066,.T.);
#2696=ORIENTED_EDGE('',*,*,#2064,.T.);
#2697=ORIENTED_EDGE('',*,*,#2066,.F.);
#2698=ORIENTED_EDGE('',*,*,#2067,.F.);
#2699=ORIENTED_EDGE('',*,*,#2068,.T.);
#2700=ORIENTED_EDGE('',*,*,#2065,.T.);
#2701=ORIENTED_EDGE('',*,*,#2068,.F.);
#2702=ORIENTED_EDGE('',*,*,#2069,.F.);
#2703=ORIENTED_EDGE('',*,*,#2070,.T.);
#2704=ORIENTED_EDGE('',*,*,#2067,.T.);
#2705=ORIENTED_EDGE('',*,*,#2070,.F.);
#2706=ORIENTED_EDGE('',*,*,#2069,.T.);
#2707=ORIENTED_EDGE('',*,*,#2071,.T.);
#2708=ORIENTED_EDGE('',*,*,#2072,.T.);
#2709=ORIENTED_EDGE('',*,*,#2073,.T.);
#2710=ORIENTED_EDGE('',*,*,#2074,.F.);
#2711=ORIENTED_EDGE('',*,*,#2075,.T.);
#2712=ORIENTED_EDGE('',*,*,#2076,.T.);
#2713=ORIENTED_EDGE('',*,*,#2077,.T.);
#2714=ORIENTED_EDGE('',*,*,#2072,.F.);
#2715=ORIENTED_EDGE('',*,*,#2078,.T.);
#2716=ORIENTED_EDGE('',*,*,#2079,.T.);
#2717=ORIENTED_EDGE('',*,*,#2080,.T.);
#2718=ORIENTED_EDGE('',*,*,#2076,.F.);
#2719=ORIENTED_EDGE('',*,*,#2081,.T.);
#2720=ORIENTED_EDGE('',*,*,#2082,.T.);
#2721=ORIENTED_EDGE('',*,*,#2083,.T.);
#2722=ORIENTED_EDGE('',*,*,#2079,.F.);
#2723=ORIENTED_EDGE('',*,*,#2084,.T.);
#2724=ORIENTED_EDGE('',*,*,#2085,.T.);
#2725=ORIENTED_EDGE('',*,*,#2086,.T.);
#2726=ORIENTED_EDGE('',*,*,#2082,.F.);
#2727=ORIENTED_EDGE('',*,*,#2087,.T.);
#2728=ORIENTED_EDGE('',*,*,#2074,.T.);
#2729=ORIENTED_EDGE('',*,*,#2088,.T.);
#2730=ORIENTED_EDGE('',*,*,#2085,.F.);
#2731=ORIENTED_EDGE('',*,*,#2087,.F.);
#2732=ORIENTED_EDGE('',*,*,#2084,.F.);
#2733=ORIENTED_EDGE('',*,*,#2081,.F.);
#2734=ORIENTED_EDGE('',*,*,#2078,.F.);
#2735=ORIENTED_EDGE('',*,*,#2075,.F.);
#2736=ORIENTED_EDGE('',*,*,#2071,.F.);
#2737=ORIENTED_EDGE('',*,*,#2088,.F.);
#2738=ORIENTED_EDGE('',*,*,#2073,.F.);
#2739=ORIENTED_EDGE('',*,*,#2077,.F.);
#2740=ORIENTED_EDGE('',*,*,#2080,.F.);
#2741=ORIENTED_EDGE('',*,*,#2083,.F.);
#2742=ORIENTED_EDGE('',*,*,#2086,.F.);
#3113=CYLINDRICAL_SURFACE('',#3757,0.65);
#3114=CYLINDRICAL_SURFACE('',#3765,0.3933);
#3231=ADVANCED_FACE('',(#614),#461,.T.);
#3232=ADVANCED_FACE('',(#615),#13,.T.);
#3233=ADVANCED_FACE('',(#616),#3113,.T.);
#3234=ADVANCED_FACE('',(#617),#14,.T.);
#3235=ADVANCED_FACE('',(#618,#393),#462,.T.);
#3236=ADVANCED_FACE('',(#619),#15,.T.);
#3237=ADVANCED_FACE('',(#620),#3114,.T.);
#3238=ADVANCED_FACE('',(#621),#16,.T.);
#3239=ADVANCED_FACE('',(#622),#463,.T.);
#3240=ADVANCED_FACE('',(#623),#464,.F.);
#3241=ADVANCED_FACE('',(#624),#465,.F.);
#3242=ADVANCED_FACE('',(#625),#466,.F.);
#3243=ADVANCED_FACE('',(#626),#467,.F.);
#3244=ADVANCED_FACE('',(#627),#468,.F.);
#3245=ADVANCED_FACE('',(#628),#469,.F.);
#3246=ADVANCED_FACE('',(#629),#470,.F.);
#3247=ADVANCED_FACE('',(#630),#471,.F.);
#3333=CLOSED_SHELL('',(#3231,#3232,#3233,#3234,#3235,#3236,#3237,#3238,
#3239));
#3334=CLOSED_SHELL('',(#3240,#3241,#3242,#3243,#3244,#3245,#3246,#3247));
#3752=AXIS2_PLACEMENT_3D('',#5820,#4442,#4443);
#3753=AXIS2_PLACEMENT_3D('',#5821,#4444,#4445);
#3754=AXIS2_PLACEMENT_3D('',#5823,#4446,#4447);
#3755=AXIS2_PLACEMENT_3D('',#5824,#4448,#4449);
#3756=AXIS2_PLACEMENT_3D('',#5826,#4450,#4451);
#3757=AXIS2_PLACEMENT_3D('',#5828,#4453,#4454);
#3758=AXIS2_PLACEMENT_3D('',#5830,#4455,#4456);
#3759=AXIS2_PLACEMENT_3D('',#5832,#4458,#4459);
#3760=AXIS2_PLACEMENT_3D('',#5834,#4460,#4461);
#3761=AXIS2_PLACEMENT_3D('',#5836,#4463,#4464);
#3762=AXIS2_PLACEMENT_3D('',#5838,#4465,#4466);
#3763=AXIS2_PLACEMENT_3D('',#5839,#4467,#4468);
#3764=AXIS2_PLACEMENT_3D('',#5841,#4469,#4470);
#3765=AXIS2_PLACEMENT_3D('',#5843,#4472,#4473);
#3766=AXIS2_PLACEMENT_3D('',#5845,#4474,#4475);
#3767=AXIS2_PLACEMENT_3D('',#5847,#4477,#4478);
#3768=AXIS2_PLACEMENT_3D('',#5849,#4479,#4480);
#3769=AXIS2_PLACEMENT_3D('',#5851,#4482,#4483);
#3770=AXIS2_PLACEMENT_3D('',#5852,#4484,#4485);
#3771=AXIS2_PLACEMENT_3D('',#5861,#4490,#4491);
#3772=AXIS2_PLACEMENT_3D('',#5867,#4495,#4496);
#3773=AXIS2_PLACEMENT_3D('',#5873,#4500,#4501);
#3774=AXIS2_PLACEMENT_3D('',#5879,#4505,#4506);
#3775=AXIS2_PLACEMENT_3D('',#5885,#4510,#4511);
#3776=AXIS2_PLACEMENT_3D('',#5888,#4514,#4515);
#3777=AXIS2_PLACEMENT_3D('',#5889,#4516,#4517);
#4442=DIRECTION('axis',(0.,0.,1.));
#4443=DIRECTION('refdir',(1.,0.,0.));
#4444=DIRECTION('center_axis',(0.,1.,0.));
#4445=DIRECTION('ref_axis',(0.,0.,1.));
#4446=DIRECTION('center_axis',(0.,-1.,0.));
#4447=DIRECTION('ref_axis',(1.,0.,0.));
#4448=DIRECTION('center_axis',(0.,-1.,0.));
#4449=DIRECTION('ref_axis',(1.,0.,0.));
#4450=DIRECTION('center_axis',(0.,-1.,0.));
#4451=DIRECTION('ref_axis',(1.,0.,0.));
#4452=DIRECTION('',(0.707106781186548,0.707106781186547,8.65956056235493E-17));
#4453=DIRECTION('center_axis',(0.,-1.,0.));
#4454=DIRECTION('ref_axis',(1.,0.,0.));
#4455=DIRECTION('center_axis',(0.,-1.,0.));
#4456=DIRECTION('ref_axis',(1.,0.,0.));
#4457=DIRECTION('',(0.,1.,0.));
#4458=DIRECTION('center_axis',(0.,1.,0.));
#4459=DIRECTION('ref_axis',(1.,0.,0.));
#4460=DIRECTION('center_axis',(0.,-1.,0.));
#4461=DIRECTION('ref_axis',(1.,0.,0.));
#4462=DIRECTION('',(-0.707106781186548,0.707106781186547,-8.65956056235494E-17));
#4463=DIRECTION('center_axis',(0.,-1.,0.));
#4464=DIRECTION('ref_axis',(0.,0.,-1.));
#4465=DIRECTION('center_axis',(0.,-1.,0.));
#4466=DIRECTION('ref_axis',(1.,0.,0.));
#4467=DIRECTION('center_axis',(0.,1.,0.));
#4468=DIRECTION('ref_axis',(1.,0.,0.));
#4469=DIRECTION('center_axis',(0.,1.,0.));
#4470=DIRECTION('ref_axis',(1.,0.,0.));
#4471=DIRECTION('',(-0.447213595499958,0.894427190999916,-5.47678698264203E-17));
#4472=DIRECTION('center_axis',(0.,-1.,0.));
#4473=DIRECTION('ref_axis',(1.,0.,0.));
#4474=DIRECTION('center_axis',(0.,1.,0.));
#4475=DIRECTION('ref_axis',(1.,0.,0.));
#4476=DIRECTION('',(0.,1.,0.));
#4477=DIRECTION('center_axis',(0.,1.,0.));
#4478=DIRECTION('ref_axis',(1.,0.,0.));
#4479=DIRECTION('center_axis',(0.,-1.,0.));
#4480=DIRECTION('ref_axis',(1.,0.,0.));
#4481=DIRECTION('',(-0.707106781186547,0.707106781186548,-8.65956056235493E-17));
#4482=DIRECTION('center_axis',(0.,-1.,0.));
#4483=DIRECTION('ref_axis',(0.,0.,-1.));
#4484=DIRECTION('center_axis',(0.866025403784439,0.,-0.5));
#4485=DIRECTION('ref_axis',(0.5,0.,0.866025403784439));
#4486=DIRECTION('',(-0.5,0.,-0.866025403784439));
#4487=DIRECTION('',(0.,-1.,0.));
#4488=DIRECTION('',(0.5,0.,0.866025403784439));
#4489=DIRECTION('',(0.,-1.,0.));
#4490=DIRECTION('center_axis',(1.60246890531964E-16,0.,-1.));
#4491=DIRECTION('ref_axis',(1.,0.,1.60246890531964E-16));
#4492=DIRECTION('',(-1.,0.,-1.60246890531964E-16));
#4493=DIRECTION('',(0.,-1.,0.));
#4494=DIRECTION('',(1.,0.,1.60246890531964E-16));
#4495=DIRECTION('center_axis',(-0.866025403784439,0.,-0.5));
#4496=DIRECTION('ref_axis',(0.5,0.,-0.866025403784439));
#4497=DIRECTION('',(-0.5,0.,0.866025403784439));
#4498=DIRECTION('',(0.,-1.,0.));
#4499=DIRECTION('',(0.5,0.,-0.866025403784439));
#4500=DIRECTION('center_axis',(-0.866025403784439,0.,0.5));
#4501=DIRECTION('ref_axis',(-0.5,0.,-0.866025403784439));
#4502=DIRECTION('',(0.5,0.,0.866025403784439));
#4503=DIRECTION('',(0.,-1.,0.));
#4504=DIRECTION('',(-0.5,0.,-0.866025403784439));
#4505=DIRECTION('center_axis',(-1.60246890531964E-16,0.,1.));
#4506=DIRECTION('ref_axis',(-1.,0.,-1.60246890531964E-16));
#4507=DIRECTION('',(1.,0.,1.60246890531964E-16));
#4508=DIRECTION('',(0.,-1.,0.));
#4509=DIRECTION('',(-1.,0.,-1.60246890531964E-16));
#4510=DIRECTION('center_axis',(0.866025403784439,0.,0.5));
#4511=DIRECTION('ref_axis',(-0.5,0.,0.866025403784439));
#4512=DIRECTION('',(0.5,0.,-0.866025403784439));
#4513=DIRECTION('',(-0.5,0.,0.866025403784439));
#4514=DIRECTION('center_axis',(0.,1.,0.));
#4515=DIRECTION('ref_axis',(1.,0.,0.));
#4516=DIRECTION('center_axis',(0.,-1.,0.));
#4517=DIRECTION('ref_axis',(0.,0.,-1.));
#5820=CARTESIAN_POINT('',(0.,0.,0.));
#5821=CARTESIAN_POINT('Origin',(0.6,0.8,0.));
#5822=CARTESIAN_POINT('',(-0.6,0.8,-7.34788079488412E-17));
#5823=CARTESIAN_POINT('Origin',(0.,0.8,0.));
#5824=CARTESIAN_POINT('Origin',(0.,0.775,0.));
#5825=CARTESIAN_POINT('',(-0.65,0.75,-7.9602041944578E-17));
#5826=CARTESIAN_POINT('Origin',(0.,0.75,0.));
#5827=CARTESIAN_POINT('',(-0.625,0.775,-7.65404249467096E-17));
#5828=CARTESIAN_POINT('Origin',(0.,0.39,0.));
#5829=CARTESIAN_POINT('',(-0.65,0.0299999999999998,-7.9602041944578E-17));
#5830=CARTESIAN_POINT('Origin',(0.,0.0299999999999998,0.));
#5831=CARTESIAN_POINT('',(-0.65,0.39,-7.9602041944578E-17));
#5832=CARTESIAN_POINT('Origin',(0.,0.0150000000000001,0.));
#5833=CARTESIAN_POINT('',(-0.62,5.89805981832114E-17,-7.59281015471359E-17));
#5834=CARTESIAN_POINT('Origin',(0.,0.,0.));
#5835=CARTESIAN_POINT('',(-0.635,0.0150000000000001,-7.77650717458569E-17));
#5836=CARTESIAN_POINT('Origin',(0.42,0.,0.));
#5837=CARTESIAN_POINT('',(-0.42,-3.46944695195361E-18,-5.14351655641888E-17));
#5838=CARTESIAN_POINT('Origin',(0.,0.,0.));
#5839=CARTESIAN_POINT('Origin',(0.,-0.02,0.));
#5840=CARTESIAN_POINT('',(-0.3933,-0.0534000000000001,4.81653586104654E-17));
#5841=CARTESIAN_POINT('Origin',(0.,-0.0534000000000001,0.));
#5842=CARTESIAN_POINT('',(-0.41,-0.02,-5.02105187650415E-17));
#5843=CARTESIAN_POINT('Origin',(0.,-1.48,0.));
#5844=CARTESIAN_POINT('',(-0.3933,-2.9267,4.81653586104654E-17));
#5845=CARTESIAN_POINT('Origin',(0.,-2.9267,0.));
#5846=CARTESIAN_POINT('',(-0.3933,-1.48,-4.81653586104654E-17));
#5847=CARTESIAN_POINT('Origin',(0.,-2.96,0.));
#5848=CARTESIAN_POINT('',(-0.32,-3.,-3.91886975727153E-17));
#5849=CARTESIAN_POINT('Origin',(0.,-3.,0.));
#5850=CARTESIAN_POINT('',(-0.36,-2.96,-4.40872847693047E-17));
#5851=CARTESIAN_POINT('Origin',(0.,-3.,0.));
#5852=CARTESIAN_POINT('Origin',(0.173205080756888,-0.8,-0.3));
#5853=CARTESIAN_POINT('',(0.346410161513775,-0.8,0.));
#5854=CARTESIAN_POINT('',(0.173205080756888,-0.8,-0.3));
#5855=CARTESIAN_POINT('',(0.346410161513775,-0.8,0.));
#5856=CARTESIAN_POINT('',(0.173205080756888,-1.28,-0.3));
#5857=CARTESIAN_POINT('',(0.173205080756888,-0.8,-0.3));
#5858=CARTESIAN_POINT('',(0.346410161513775,-1.28,0.));
#5859=CARTESIAN_POINT('',(0.346410161513775,-1.28,0.));
#5860=CARTESIAN_POINT('',(0.346410161513775,-0.8,0.));
#5861=CARTESIAN_POINT('Origin',(-0.173205080756888,-0.8,-0.3));
#5862=CARTESIAN_POINT('',(-0.173205080756888,-0.8,-0.3));
#5863=CARTESIAN_POINT('',(0.173205080756888,-0.8,-0.3));
#5864=CARTESIAN_POINT('',(-0.173205080756888,-1.28,-0.3));
#5865=CARTESIAN_POINT('',(-0.173205080756888,-0.8,-0.3));
#5866=CARTESIAN_POINT('',(0.173205080756888,-1.28,-0.3));
#5867=CARTESIAN_POINT('Origin',(-0.346410161513775,-0.8,-5.55111512312578E-17));
#5868=CARTESIAN_POINT('',(-0.346410161513775,-0.8,-4.24230095489963E-17));
#5869=CARTESIAN_POINT('',(-0.173205080756888,-0.8,-0.3));
#5870=CARTESIAN_POINT('',(-0.346410161513775,-1.28,-5.55111512312578E-17));
#5871=CARTESIAN_POINT('',(-0.346410161513775,-0.8,-4.24230095489963E-17));
#5872=CARTESIAN_POINT('',(-0.173205080756888,-1.28,-0.3));
#5873=CARTESIAN_POINT('Origin',(-0.173205080756888,-0.8,0.3));
#5874=CARTESIAN_POINT('',(-0.173205080756888,-0.8,0.3));
#5875=CARTESIAN_POINT('',(-0.346410161513775,-0.8,-4.24230095489963E-17));
#5876=CARTESIAN_POINT('',(-0.173205080756888,-1.28,0.3));
#5877=CARTESIAN_POINT('',(-0.173205080756888,-0.8,0.3));
#5878=CARTESIAN_POINT('',(-0.346410161513775,-1.28,-4.24230095489963E-17));
#5879=CARTESIAN_POINT('Origin',(0.173205080756888,-0.8,0.3));
#5880=CARTESIAN_POINT('',(0.173205080756888,-0.8,0.3));
#5881=CARTESIAN_POINT('',(-0.173205080756888,-0.8,0.3));
#5882=CARTESIAN_POINT('',(0.173205080756888,-1.28,0.3));
#5883=CARTESIAN_POINT('',(0.173205080756888,-0.8,0.3));
#5884=CARTESIAN_POINT('',(-0.173205080756888,-1.28,0.3));
#5885=CARTESIAN_POINT('Origin',(0.346410161513775,-0.8,0.));
#5886=CARTESIAN_POINT('',(0.173205080756888,-0.8,0.3));
#5887=CARTESIAN_POINT('',(0.173205080756888,-1.28,0.3));
#5888=CARTESIAN_POINT('Origin',(0.,-0.8,-5.55111512312578E-17));
#5889=CARTESIAN_POINT('Origin',(0.,-1.28,-5.55111512312578E-17));
#6771=UNCERTAINTY_MEASURE_WITH_UNIT(LENGTH_MEASURE(0.001),#6806,
'DISTANCE_ACCURACY_VALUE',
'Maximum model space distance between geometric entities at asserted c
onnectivities');
#6780=UNCERTAINTY_MEASURE_WITH_UNIT(LENGTH_MEASURE(0.001),#6806,
'DISTANCE_ACCURACY_VALUE',
'Maximum model space distance between geometric entities at asserted c
onnectivities');
#6796=(
GEOMETRIC_REPRESENTATION_CONTEXT(3)
GLOBAL_UNCERTAINTY_ASSIGNED_CONTEXT((#6771))
GLOBAL_UNIT_ASSIGNED_CONTEXT((#6806,#6808,#6809))
REPRESENTATION_CONTEXT('','3D')
);
#6805=(
GEOMETRIC_REPRESENTATION_CONTEXT(3)
GLOBAL_UNCERTAINTY_ASSIGNED_CONTEXT((#6780))
GLOBAL_UNIT_ASSIGNED_CONTEXT((#6806,#6808,#6809))
REPRESENTATION_CONTEXT('','3D')
);
#6806=(
LENGTH_UNIT()
NAMED_UNIT(*)
SI_UNIT(.CENTI.,.METRE.)
);
#6808=(
NAMED_UNIT(*)
PLANE_ANGLE_UNIT()
SI_UNIT($,.RADIAN.)
);
#6809=(
NAMED_UNIT(*)
SI_UNIT($,.STERADIAN.)
SOLID_ANGLE_UNIT()
);
#6825=SHAPE_DEFINITION_REPRESENTATION(#6851,#6913);
#6851=PRODUCT_DEFINITION_SHAPE('',$,#6938);
#6913=SHAPE_REPRESENTATION('',(#3752),#6796);
#6922=PRODUCT_DEFINITION_CONTEXT('part definition',#6996,'design');
#6938=PRODUCT_DEFINITION('Cap Screw - M8x30','Cap Screw - M8x30',#6962,
#6922);
#6962=PRODUCT_DEFINITION_FORMATION('',$,#7013);
#6996=APPLICATION_CONTEXT(
'Core Data for Automotive Mechanical Design Process');
#6997=PRODUCT_CONTEXT('part definition',#6996,'mechanical');
#7013=PRODUCT('Cap Screw - M8x30','Cap Screw - M8x30',
'Cap Screw - M8x30',(#6997));
#7092=COLOUR_RGB('Black',0.12,0.14,0.17);
#7093=FILL_AREA_STYLE_COLOUR('',#7092);
#7094=FILL_AREA_STYLE('',(#7093));
#7095=SURFACE_STYLE_FILL_AREA(#7094);
#7096=SURFACE_SIDE_STYLE('',(#7095));
#7097=SURFACE_STYLE_USAGE(.BOTH.,#7096);
#7098=PRESENTATION_STYLE_ASSIGNMENT((#7097));
ENDSEC;
END-ISO-10303-21;
